ISO-10303-21;
HEADER;
/* Generated by software containing ST-Developer
 * from STEP Tools, Inc. (www.steptools.com) 
 */

FILE_DESCRIPTION(
/* description */ ('PAT-091'),
/* implementation_level */ '2;1');

FILE_NAME(
/* name */ 'Centre bearing retainer (2).step',
/* time_stamp */ '2026-10-27T15:34:44-07:00',
/* author */ (''),
/* organization */ (''),
/* preprocessor_version */ 'ST-DEVELOPER v20.2',
/* originating_system */ 'Autodesk Translation Framework v15.17.0.0',
/* authorisation */ '');

FILE_SCHEMA (('AUTOMOTIVE_DESIGN { 1 0 10303 214 3 1 1 }'));
ENDSEC;

DATA;
#10=MECHANICAL_DESIGN_GEOMETRIC_PRESENTATION_REPRESENTATION('',(#1060),#25100);
#840=SHAPE_REPRESENTATION_RELATIONSHIP('SRR','None',#25607,#950);
#950=ADVANCED_BREP_SHAPE_REPRESENTATION('',(#1181),#25077);
#1060=STYLED_ITEM('',(#26191),#1181);
#1181=MANIFOLD_SOLID_BREP('Body1',#13340);
#1589=FACE_BOUND('',#3918,.T.);
#1590=FACE_BOUND('',#3919,.T.);
#1591=FACE_BOUND('',#3920,.T.);
#1592=FACE_BOUND('',#3921,.T.);
#1593=FACE_BOUND('',#3922,.T.);
#1594=FACE_BOUND('',#3924,.T.);
#1595=FACE_BOUND('',#3925,.T.);
#1596=FACE_BOUND('',#3926,.T.);
#1597=FACE_BOUND('',#3927,.T.);
#1598=FACE_BOUND('',#3928,.T.);
#1996=PLANE('',#16029);
#1997=PLANE('',#16030);
#2719=FACE_OUTER_BOUND('',#3911,.T.);
#2720=FACE_OUTER_BOUND('',#3912,.T.);
#2721=FACE_OUTER_BOUND('',#3913,.T.);
#2722=FACE_OUTER_BOUND('',#3914,.T.);
#2723=FACE_OUTER_BOUND('',#3915,.T.);
#2724=FACE_OUTER_BOUND('',#3916,.T.);
#2725=FACE_OUTER_BOUND('',#3917,.T.);
#2726=FACE_OUTER_BOUND('',#3923,.T.);
#3911=EDGE_LOOP('',(#11540,#11541,#11542,#11543));
#3912=EDGE_LOOP('',(#11544,#11545,#11546,#11547));
#3913=EDGE_LOOP('',(#11548,#11549,#11550,#11551));
#3914=EDGE_LOOP('',(#11552,#11553,#11554,#11555));
#3915=EDGE_LOOP('',(#11556,#11557,#11558,#11559));
#3916=EDGE_LOOP('',(#11560,#11561,#11562,#11563));
#3917=EDGE_LOOP('',(#11564));
#3918=EDGE_LOOP('',(#11565));
#3919=EDGE_LOOP('',(#11566));
#3920=EDGE_LOOP('',(#11567));
#3921=EDGE_LOOP('',(#11568));
#3922=EDGE_LOOP('',(#11569));
#3923=EDGE_LOOP('',(#11570));
#3924=EDGE_LOOP('',(#11571));
#3925=EDGE_LOOP('',(#11572));
#3926=EDGE_LOOP('',(#11573));
#3927=EDGE_LOOP('',(#11574));
#3928=EDGE_LOOP('',(#11575));
#4806=LINE('',#23994,#5546);
#4807=LINE('',#24000,#5547);
#4808=LINE('',#24006,#5548);
#4809=LINE('',#24012,#5549);
#4810=LINE('',#24018,#5550);
#4811=LINE('',#24024,#5551);
#5546=VECTOR('',#20006,0.225000000000001);
#5547=VECTOR('',#20013,0.225000000000001);
#5548=VECTOR('',#20020,0.225000000000001);
#5549=VECTOR('',#20027,0.225000000000001);
#5550=VECTOR('',#20034,1.02);
#5551=VECTOR('',#20041,2.2);
#6202=CIRCLE('',#16012,0.225000000000001);
#6203=CIRCLE('',#16013,0.225000000000001);
#6204=CIRCLE('',#16015,0.225000000000001);
#6205=CIRCLE('',#16016,0.225000000000001);
#6206=CIRCLE('',#16018,0.225000000000001);
#6207=CIRCLE('',#16019,0.225000000000001);
#6208=CIRCLE('',#16021,0.225000000000001);
#6209=CIRCLE('',#16022,0.225000000000001);
#6210=CIRCLE('',#16024,1.02);
#6211=CIRCLE('',#16025,1.02);
#6212=CIRCLE('',#16027,2.2);
#6213=CIRCLE('',#16028,2.2);
#7235=VERTEX_POINT('',#23991);
#7236=VERTEX_POINT('',#23993);
#7237=VERTEX_POINT('',#23997);
#7238=VERTEX_POINT('',#23999);
#7239=VERTEX_POINT('',#24003);
#7240=VERTEX_POINT('',#24005);
#7241=VERTEX_POINT('',#24009);
#7242=VERTEX_POINT('',#24011);
#7243=VERTEX_POINT('',#24015);
#7244=VERTEX_POINT('',#24017);
#7245=VERTEX_POINT('',#24021);
#7246=VERTEX_POINT('',#24023);
#8705=EDGE_CURVE('',#7235,#7235,#6202,.T.);
#8706=EDGE_CURVE('',#7235,#7236,#4806,.T.);
#8707=EDGE_CURVE('',#7236,#7236,#6203,.T.);
#8708=EDGE_CURVE('',#7237,#7237,#6204,.T.);
#8709=EDGE_CURVE('',#7237,#7238,#4807,.T.);
#8710=EDGE_CURVE('',#7238,#7238,#6205,.T.);
#8711=EDGE_CURVE('',#7239,#7239,#6206,.T.);
#8712=EDGE_CURVE('',#7239,#7240,#4808,.T.);
#8713=EDGE_CURVE('',#7240,#7240,#6207,.T.);
#8714=EDGE_CURVE('',#7241,#7241,#6208,.T.);
#8715=EDGE_CURVE('',#7241,#7242,#4809,.T.);
#8716=EDGE_CURVE('',#7242,#7242,#6209,.T.);
#8717=EDGE_CURVE('',#7243,#7243,#6210,.T.);
#8718=EDGE_CURVE('',#7243,#7244,#4810,.T.);
#8719=EDGE_CURVE('',#7244,#7244,#6211,.T.);
#8720=EDGE_CURVE('',#7245,#7245,#6212,.T.);
#8721=EDGE_CURVE('',#7245,#7246,#4811,.T.);
#8722=EDGE_CURVE('',#7246,#7246,#6213,.T.);
#11540=ORIENTED_EDGE('',*,*,#8705,.F.);
#11541=ORIENTED_EDGE('',*,*,#8706,.T.);
#11542=ORIENTED_EDGE('',*,*,#8707,.F.);
#11543=ORIENTED_EDGE('',*,*,#8706,.F.);
#11544=ORIENTED_EDGE('',*,*,#8708,.F.);
#11545=ORIENTED_EDGE('',*,*,#8709,.T.);
#11546=ORIENTED_EDGE('',*,*,#8710,.F.);
#11547=ORIENTED_EDGE('',*,*,#8709,.F.);
#11548=ORIENTED_EDGE('',*,*,#8711,.F.);
#11549=ORIENTED_EDGE('',*,*,#8712,.T.);
#11550=ORIENTED_EDGE('',*,*,#8713,.F.);
#11551=ORIENTED_EDGE('',*,*,#8712,.F.);
#11552=ORIENTED_EDGE('',*,*,#8714,.F.);
#11553=ORIENTED_EDGE('',*,*,#8715,.T.);
#11554=ORIENTED_EDGE('',*,*,#8716,.F.);
#11555=ORIENTED_EDGE('',*,*,#8715,.F.);
#11556=ORIENTED_EDGE('',*,*,#8717,.F.);
#11557=ORIENTED_EDGE('',*,*,#8718,.T.);
#11558=ORIENTED_EDGE('',*,*,#8719,.T.);
#11559=ORIENTED_EDGE('',*,*,#8718,.F.);
#11560=ORIENTED_EDGE('',*,*,#8720,.F.);
#11561=ORIENTED_EDGE('',*,*,#8721,.T.);
#11562=ORIENTED_EDGE('',*,*,#8722,.T.);
#11563=ORIENTED_EDGE('',*,*,#8721,.F.);
#11564=ORIENTED_EDGE('',*,*,#8720,.T.);
#11565=ORIENTED_EDGE('',*,*,#8717,.T.);
#11566=ORIENTED_EDGE('',*,*,#8716,.T.);
#11567=ORIENTED_EDGE('',*,*,#8713,.T.);
#11568=ORIENTED_EDGE('',*,*,#8710,.T.);
#11569=ORIENTED_EDGE('',*,*,#8707,.T.);
#11570=ORIENTED_EDGE('',*,*,#8722,.F.);
#11571=ORIENTED_EDGE('',*,*,#8719,.F.);
#11572=ORIENTED_EDGE('',*,*,#8714,.T.);
#11573=ORIENTED_EDGE('',*,*,#8711,.T.);
#11574=ORIENTED_EDGE('',*,*,#8708,.T.);
#11575=ORIENTED_EDGE('',*,*,#8705,.T.);
#12362=CYLINDRICAL_SURFACE('',#16011,0.225000000000001);
#12363=CYLINDRICAL_SURFACE('',#16014,0.225000000000001);
#12364=CYLINDRICAL_SURFACE('',#16017,0.225000000000001);
#12365=CYLINDRICAL_SURFACE('',#16020,0.225000000000001);
#12366=CYLINDRICAL_SURFACE('',#16023,1.02);
#12367=CYLINDRICAL_SURFACE('',#16026,2.2);
#13086=ADVANCED_FACE('',(#2719),#12362,.F.);
#13087=ADVANCED_FACE('',(#2720),#12363,.F.);
#13088=ADVANCED_FACE('',(#2721),#12364,.F.);
#13089=ADVANCED_FACE('',(#2722),#12365,.F.);
#13090=ADVANCED_FACE('',(#2723),#12366,.F.);
#13091=ADVANCED_FACE('',(#2724),#12367,.T.);
#13092=ADVANCED_FACE('',(#2725,#1589,#1590,#1591,#1592,#1593),#1996,.T.);
#13093=ADVANCED_FACE('',(#2726,#1594,#1595,#1596,#1597,#1598),#1997,.F.);
#13340=CLOSED_SHELL('',(#13086,#13087,#13088,#13089,#13090,#13091,#13092,
#13093));
#16010=AXIS2_PLACEMENT_3D('',#23989,#20000,#20001);
#16011=AXIS2_PLACEMENT_3D('',#23990,#20002,#20003);
#16012=AXIS2_PLACEMENT_3D('',#23992,#20004,#20005);
#16013=AXIS2_PLACEMENT_3D('',#23995,#20007,#20008);
#16014=AXIS2_PLACEMENT_3D('',#23996,#20009,#20010);
#16015=AXIS2_PLACEMENT_3D('',#23998,#20011,#20012);
#16016=AXIS2_PLACEMENT_3D('',#24001,#20014,#20015);
#16017=AXIS2_PLACEMENT_3D('',#24002,#20016,#20017);
#16018=AXIS2_PLACEMENT_3D('',#24004,#20018,#20019);
#16019=AXIS2_PLACEMENT_3D('',#24007,#20021,#20022);
#16020=AXIS2_PLACEMENT_3D('',#24008,#20023,#20024);
#16021=AXIS2_PLACEMENT_3D('',#24010,#20025,#20026);
#16022=AXIS2_PLACEMENT_3D('',#24013,#20028,#20029);
#16023=AXIS2_PLACEMENT_3D('',#24014,#20030,#20031);
#16024=AXIS2_PLACEMENT_3D('',#24016,#20032,#20033);
#16025=AXIS2_PLACEMENT_3D('',#24019,#20035,#20036);
#16026=AXIS2_PLACEMENT_3D('',#24020,#20037,#20038);
#16027=AXIS2_PLACEMENT_3D('',#24022,#20039,#20040);
#16028=AXIS2_PLACEMENT_3D('',#24025,#20042,#20043);
#16029=AXIS2_PLACEMENT_3D('',#24026,#20044,#20045);
#16030=AXIS2_PLACEMENT_3D('',#24027,#20046,#20047);
#20000=DIRECTION('axis',(0.,0.,1.));
#20001=DIRECTION('refdir',(1.,0.,0.));
#20002=DIRECTION('center_axis',(0.,1.,0.));
#20003=DIRECTION('ref_axis',(1.,0.,0.));
#20004=DIRECTION('center_axis',(0.,1.,0.));
#20005=DIRECTION('ref_axis',(1.,0.,0.));
#20006=DIRECTION('',(0.,1.,0.));
#20007=DIRECTION('center_axis',(0.,-1.,0.));
#20008=DIRECTION('ref_axis',(1.,0.,0.));
#20009=DIRECTION('center_axis',(0.,1.,0.));
#20010=DIRECTION('ref_axis',(1.,0.,0.));
#20011=DIRECTION('center_axis',(0.,1.,0.));
#20012=DIRECTION('ref_axis',(1.,0.,0.));
#20013=DIRECTION('',(0.,1.,0.));
#20014=DIRECTION('center_axis',(0.,-1.,0.));
#20015=DIRECTION('ref_axis',(1.,0.,0.));
#20016=DIRECTION('center_axis',(0.,1.,0.));
#20017=DIRECTION('ref_axis',(1.,0.,0.));
#20018=DIRECTION('center_axis',(0.,1.,0.));
#20019=DIRECTION('ref_axis',(1.,0.,0.));
#20020=DIRECTION('',(0.,1.,0.));
#20021=DIRECTION('center_axis',(0.,-1.,0.));
#20022=DIRECTION('ref_axis',(1.,0.,0.));
#20023=DIRECTION('center_axis',(0.,1.,0.));
#20024=DIRECTION('ref_axis',(1.,0.,0.));
#20025=DIRECTION('center_axis',(0.,1.,0.));
#20026=DIRECTION('ref_axis',(1.,0.,0.));
#20027=DIRECTION('',(0.,1.,0.));
#20028=DIRECTION('center_axis',(0.,-1.,0.));
#20029=DIRECTION('ref_axis',(1.,0.,0.));
#20030=DIRECTION('center_axis',(0.,1.,0.));
#20031=DIRECTION('ref_axis',(1.,0.,0.));
#20032=DIRECTION('center_axis',(0.,-1.,0.));
#20033=DIRECTION('ref_axis',(1.,0.,0.));
#20034=DIRECTION('',(0.,-1.,0.));
#20035=DIRECTION('center_axis',(0.,-1.,0.));
#20036=DIRECTION('ref_axis',(1.,0.,0.));
#20037=DIRECTION('center_axis',(0.,1.,0.));
#20038=DIRECTION('ref_axis',(1.,0.,0.));
#20039=DIRECTION('center_axis',(0.,1.,0.));
#20040=DIRECTION('ref_axis',(1.,0.,0.));
#20041=DIRECTION('',(0.,-1.,0.));
#20042=DIRECTION('center_axis',(0.,1.,0.));
#20043=DIRECTION('ref_axis',(1.,0.,0.));
#20044=DIRECTION('center_axis',(0.,1.,0.));
#20045=DIRECTION('ref_axis',(1.,0.,0.));
#20046=DIRECTION('center_axis',(0.,1.,0.));
#20047=DIRECTION('ref_axis',(1.,0.,0.));
#23989=CARTESIAN_POINT('',(0.,0.,0.));
#23990=CARTESIAN_POINT('Origin',(18.056769185842,6.6,6.69185245480489));
#23991=CARTESIAN_POINT('',(17.831769185842,6.7,6.69185245480489));
#23992=CARTESIAN_POINT('Origin',(18.056769185842,6.7,6.69185245480489));
#23993=CARTESIAN_POINT('',(17.831769185842,7.,6.69185245480489));
#23994=CARTESIAN_POINT('',(17.831769185842,6.6,6.69185245480489));
#23995=CARTESIAN_POINT('Origin',(18.056769185842,7.,6.69185245480489));
#23996=CARTESIAN_POINT('Origin',(18.056769185842,6.6,9.30814754519511));
#23997=CARTESIAN_POINT('',(17.831769185842,6.7,9.30814754519511));
#23998=CARTESIAN_POINT('Origin',(18.056769185842,6.7,9.30814754519511));
#23999=CARTESIAN_POINT('',(17.831769185842,7.,9.30814754519511));
#24000=CARTESIAN_POINT('',(17.831769185842,6.6,9.30814754519511));
#24001=CARTESIAN_POINT('Origin',(18.056769185842,7.,9.30814754519511));
#24002=CARTESIAN_POINT('Origin',(20.6730642762322,6.6,9.30814754519511));
#24003=CARTESIAN_POINT('',(20.4480642762322,6.7,9.30814754519511));
#24004=CARTESIAN_POINT('Origin',(20.6730642762322,6.7,9.30814754519511));
#24005=CARTESIAN_POINT('',(20.4480642762322,7.,9.30814754519511));
#24006=CARTESIAN_POINT('',(20.4480642762322,6.6,9.30814754519511));
#24007=CARTESIAN_POINT('Origin',(20.6730642762322,7.,9.30814754519511));
#24008=CARTESIAN_POINT('Origin',(20.6730642762322,6.6,6.69185245480489));
#24009=CARTESIAN_POINT('',(20.4480642762322,6.7,6.69185245480489));
#24010=CARTESIAN_POINT('Origin',(20.6730642762322,6.7,6.69185245480489));
#24011=CARTESIAN_POINT('',(20.4480642762322,7.,6.69185245480489));
#24012=CARTESIAN_POINT('',(20.4480642762322,6.6,6.69185245480489));
#24013=CARTESIAN_POINT('Origin',(20.6730642762322,7.,6.69185245480489));
#24014=CARTESIAN_POINT('Origin',(19.3649167310371,6.7,8.));
#24015=CARTESIAN_POINT('',(18.3449167310371,7.,8.));
#24016=CARTESIAN_POINT('Origin',(19.3649167310371,7.,8.));
#24017=CARTESIAN_POINT('',(18.3449167310371,6.7,8.));
#24018=CARTESIAN_POINT('',(18.3449167310371,6.7,8.));
#24019=CARTESIAN_POINT('Origin',(19.3649167310371,6.7,8.));
#24020=CARTESIAN_POINT('Origin',(19.3649167310371,6.7,8.));
#24021=CARTESIAN_POINT('',(17.1649167310371,7.,8.));
#24022=CARTESIAN_POINT('Origin',(19.3649167310371,7.,8.));
#24023=CARTESIAN_POINT('',(17.1649167310371,6.7,8.));
#24024=CARTESIAN_POINT('',(17.1649167310371,6.7,8.));
#24025=CARTESIAN_POINT('Origin',(19.3649167310371,6.7,8.));
#24026=CARTESIAN_POINT('Origin',(19.3649167310371,7.,8.));
#24027=CARTESIAN_POINT('Origin',(19.3649167310371,6.7,8.));
#24956=UNCERTAINTY_MEASURE_WITH_UNIT(LENGTH_MEASURE(0.001),#25101,
'DISTANCE_ACCURACY_VALUE',
'Maximum model space distance between geometric entities at asserted c
onnectivities');
#24979=UNCERTAINTY_MEASURE_WITH_UNIT(LENGTH_MEASURE(0.001),#25101,
'DISTANCE_ACCURACY_VALUE',
'Maximum model space distance between geometric entities at asserted c
onnectivities');
#25077=(
GEOMETRIC_REPRESENTATION_CONTEXT(3)
GLOBAL_UNCERTAINTY_ASSIGNED_CONTEXT((#24956))
GLOBAL_UNIT_ASSIGNED_CONTEXT((#25101,#25103,#25104))
REPRESENTATION_CONTEXT('','3D')
);
#25100=(
GEOMETRIC_REPRESENTATION_CONTEXT(3)
GLOBAL_UNCERTAINTY_ASSIGNED_CONTEXT((#24979))
GLOBAL_UNIT_ASSIGNED_CONTEXT((#25101,#25103,#25104))
REPRESENTATION_CONTEXT('','3D')
);
#25101=(
LENGTH_UNIT()
NAMED_UNIT(*)
SI_UNIT(.CENTI.,.METRE.)
);
#25103=(
NAMED_UNIT(*)
PLANE_ANGLE_UNIT()
SI_UNIT($,.RADIAN.)
);
#25104=(
NAMED_UNIT(*)
SI_UNIT($,.STERADIAN.)
SOLID_ANGLE_UNIT()
);
#25202=SHAPE_DEFINITION_REPRESENTATION(#25396,#25607);
#25396=PRODUCT_DEFINITION_SHAPE('',$,#25728);
#25607=SHAPE_REPRESENTATION('',(#16010),#25077);
#25630=PRODUCT_DEFINITION_CONTEXT('part definition',#25992,'design');
#25728=PRODUCT_DEFINITION('Centre bearing retainer (2)',
'Centre bearing retainer (2)',#25848,#25630);
#25848=PRODUCT_DEFINITION_FORMATION('',$,#26091);
#25992=APPLICATION_CONTEXT(
'Core Data for Automotive Mechanical Design Process');
#25993=PRODUCT_CONTEXT('part definition',#25992,'mechanical');
#26091=PRODUCT('Centre bearing retainer (2)',
'Centre bearing retainer (2)','Centre bearing retainer (2)',(#25993));
#26185=COLOUR_RGB('Grey',0.48,0.52,0.57);
#26186=FILL_AREA_STYLE_COLOUR('',#26185);
#26187=FILL_AREA_STYLE('',(#26186));
#26188=SURFACE_STYLE_FILL_AREA(#26187);
#26189=SURFACE_SIDE_STYLE('',(#26188));
#26190=SURFACE_STYLE_USAGE(.BOTH.,#26189);
#26191=PRESENTATION_STYLE_ASSIGNMENT((#26190));
ENDSEC;
END-ISO-10303-21;
